ISO-10303-21;
HEADER;
/* Generated by software containing ST-Developer
 * from STEP Tools, Inc. (www.steptools.com) 
 */

FILE_DESCRIPTION(
/* description */ ('Independent hinged machine back cover with retained hinge pins, perim
eter gasket and quarter-turn cam latch. Nominal cover 360 x 260 x 3 mm
, frame 430 x 300 x 20 mm. No guarding, structural or ingress rating a
ssigned.'),
/* implementation_level */ '2;1');

FILE_NAME(
/* name */ 'Flat washer M4.step',
/* time_stamp */ '2026-11-09T19:36:59-08:00',
/* author */ (''),
/* organization */ (''),
/* preprocessor_version */ 'ST-DEVELOPER v20.2',
/* originating_system */ 'Autodesk Translation Framework v15.17.0.0',
/* authorisation */ '');

FILE_SCHEMA (('AUTOMOTIVE_DESIGN { 1 0 10303 214 3 1 1 }'));
ENDSEC;

DATA;
#10=MECHANICAL_DESIGN_GEOMETRIC_PRESENTATION_REPRESENTATION('',(#205),#32627);
#169=SHAPE_REPRESENTATION_RELATIONSHIP('SRR','None',#32715,#187);
#187=ADVANCED_BREP_SHAPE_REPRESENTATION('',(#223),#32616);
#205=STYLED_ITEM('',(#32812),#223);
#223=MANIFOLD_SOLID_BREP('Body1',#8682);
#262=FACE_BOUND('',#1229,.T.);
#263=FACE_BOUND('',#1231,.T.);
#382=PLANE('',#9223);
#383=PLANE('',#9224);
#723=FACE_OUTER_BOUND('',#1226,.T.);
#724=FACE_OUTER_BOUND('',#1227,.T.);
#725=FACE_OUTER_BOUND('',#1228,.T.);
#726=FACE_OUTER_BOUND('',#1230,.T.);
#1226=EDGE_LOOP('',(#6849,#6850,#6851,#6852));
#1227=EDGE_LOOP('',(#6853,#6854,#6855,#6856));
#1228=EDGE_LOOP('',(#6857));
#1229=EDGE_LOOP('',(#6858));
#1230=EDGE_LOOP('',(#6859));
#1231=EDGE_LOOP('',(#6860));
#1516=CIRCLE('',#9218,2.5);
#1517=CIRCLE('',#9219,2.5);
#1518=CIRCLE('',#9221,4.5);
#1519=CIRCLE('',#9222,4.5);
#2486=LINE('',#24312,#3032);
#2487=LINE('',#24318,#3033);
#3032=VECTOR('',#10494,2.5);
#3033=VECTOR('',#10501,4.5);
#3761=VERTEX_POINT('',#24309);
#3762=VERTEX_POINT('',#24311);
#3763=VERTEX_POINT('',#24315);
#3764=VERTEX_POINT('',#24317);
#4848=EDGE_CURVE('',#3761,#3761,#1516,.T.);
#4849=EDGE_CURVE('',#3761,#3762,#2486,.T.);
#4850=EDGE_CURVE('',#3762,#3762,#1517,.T.);
#4851=EDGE_CURVE('',#3763,#3763,#1518,.T.);
#4852=EDGE_CURVE('',#3763,#3764,#2487,.T.);
#4853=EDGE_CURVE('',#3764,#3764,#1519,.T.);
#6849=ORIENTED_EDGE('',*,*,#4848,.F.);
#6850=ORIENTED_EDGE('',*,*,#4849,.T.);
#6851=ORIENTED_EDGE('',*,*,#4850,.T.);
#6852=ORIENTED_EDGE('',*,*,#4849,.F.);
#6853=ORIENTED_EDGE('',*,*,#4851,.F.);
#6854=ORIENTED_EDGE('',*,*,#4852,.T.);
#6855=ORIENTED_EDGE('',*,*,#4853,.T.);
#6856=ORIENTED_EDGE('',*,*,#4852,.F.);
#6857=ORIENTED_EDGE('',*,*,#4851,.T.);
#6858=ORIENTED_EDGE('',*,*,#4848,.T.);
#6859=ORIENTED_EDGE('',*,*,#4853,.F.);
#6860=ORIENTED_EDGE('',*,*,#4850,.F.);
#8077=CYLINDRICAL_SURFACE('',#9217,2.5);
#8078=CYLINDRICAL_SURFACE('',#9220,4.5);
#8471=ADVANCED_FACE('',(#723),#8077,.F.);
#8472=ADVANCED_FACE('',(#724),#8078,.T.);
#8473=ADVANCED_FACE('',(#725,#262),#382,.T.);
#8474=ADVANCED_FACE('',(#726,#263),#383,.F.);
#8682=CLOSED_SHELL('',(#8471,#8472,#8473,#8474));
#9216=AXIS2_PLACEMENT_3D('',#24307,#10488,#10489);
#9217=AXIS2_PLACEMENT_3D('',#24308,#10490,#10491);
#9218=AXIS2_PLACEMENT_3D('',#24310,#10492,#10493);
#9219=AXIS2_PLACEMENT_3D('',#24313,#10495,#10496);
#9220=AXIS2_PLACEMENT_3D('',#24314,#10497,#10498);
#9221=AXIS2_PLACEMENT_3D('',#24316,#10499,#10500);
#9222=AXIS2_PLACEMENT_3D('',#24319,#10502,#10503);
#9223=AXIS2_PLACEMENT_3D('',#24320,#10504,#10505);
#9224=AXIS2_PLACEMENT_3D('',#24321,#10506,#10507);
#10488=DIRECTION('axis',(0.,0.,1.));
#10489=DIRECTION('refdir',(1.,0.,0.));
#10490=DIRECTION('center_axis',(0.,0.,1.));
#10491=DIRECTION('ref_axis',(1.,0.,0.));
#10492=DIRECTION('center_axis',(0.,0.,-1.));
#10493=DIRECTION('ref_axis',(1.,0.,0.));
#10494=DIRECTION('',(0.,0.,-1.));
#10495=DIRECTION('center_axis',(0.,0.,-1.));
#10496=DIRECTION('ref_axis',(1.,0.,0.));
#10497=DIRECTION('center_axis',(0.,0.,1.));
#10498=DIRECTION('ref_axis',(1.,0.,0.));
#10499=DIRECTION('center_axis',(0.,0.,1.));
#10500=DIRECTION('ref_axis',(1.,0.,0.));
#10501=DIRECTION('',(0.,0.,-1.));
#10502=DIRECTION('center_axis',(0.,0.,1.));
#10503=DIRECTION('ref_axis',(1.,0.,0.));
#10504=DIRECTION('center_axis',(0.,0.,1.));
#10505=DIRECTION('ref_axis',(1.,0.,0.));
#10506=DIRECTION('center_axis',(0.,0.,1.));
#10507=DIRECTION('ref_axis',(1.,0.,0.));
#24307=CARTESIAN_POINT('',(0.,0.,0.));
#24308=CARTESIAN_POINT('Origin',(0.,0.,0.));
#24309=CARTESIAN_POINT('',(-2.5,-3.06161699786838E-16,1.));
#24310=CARTESIAN_POINT('Origin',(0.,0.,1.));
#24311=CARTESIAN_POINT('',(-2.5,-3.06161699786838E-16,0.));
#24312=CARTESIAN_POINT('',(-2.5,-3.06161699786838E-16,0.));
#24313=CARTESIAN_POINT('Origin',(0.,0.,0.));
#24314=CARTESIAN_POINT('Origin',(0.,0.,0.));
#24315=CARTESIAN_POINT('',(-4.5,-5.51091059616309E-16,1.));
#24316=CARTESIAN_POINT('Origin',(0.,0.,1.));
#24317=CARTESIAN_POINT('',(-4.5,-5.51091059616309E-16,0.));
#24318=CARTESIAN_POINT('',(-4.5,-5.51091059616309E-16,0.));
#24319=CARTESIAN_POINT('Origin',(0.,0.,0.));
#24320=CARTESIAN_POINT('Origin',(0.,0.,1.));
#24321=CARTESIAN_POINT('Origin',(0.,0.,0.));
#32596=UNCERTAINTY_MEASURE_WITH_UNIT(LENGTH_MEASURE(0.01),#32628,
'DISTANCE_ACCURACY_VALUE',
'Maximum model space distance between geometric entities at asserted c
onnectivities');
#32607=UNCERTAINTY_MEASURE_WITH_UNIT(LENGTH_MEASURE(0.01),#32628,
'DISTANCE_ACCURACY_VALUE',
'Maximum model space distance between geometric entities at asserted c
onnectivities');
#32616=(
GEOMETRIC_REPRESENTATION_CONTEXT(3)
GLOBAL_UNCERTAINTY_ASSIGNED_CONTEXT((#32596))
GLOBAL_UNIT_ASSIGNED_CONTEXT((#32628,#32630,#32631))
REPRESENTATION_CONTEXT('','3D')
);
#32627=(
GEOMETRIC_REPRESENTATION_CONTEXT(3)
GLOBAL_UNCERTAINTY_ASSIGNED_CONTEXT((#32607))
GLOBAL_UNIT_ASSIGNED_CONTEXT((#32628,#32630,#32631))
REPRESENTATION_CONTEXT('','3D')
);
#32628=(
LENGTH_UNIT()
NAMED_UNIT(*)
SI_UNIT(.MILLI.,.METRE.)
);
#32630=(
NAMED_UNIT(*)
PLANE_ANGLE_UNIT()
SI_UNIT($,.RADIAN.)
);
#32631=(
NAMED_UNIT(*)
SI_UNIT($,.STERADIAN.)
SOLID_ANGLE_UNIT()
);
#32640=SHAPE_DEFINITION_REPRESENTATION(#32659,#32715);
#32659=PRODUCT_DEFINITION_SHAPE('',$,#32735);
#32715=SHAPE_REPRESENTATION('',(#9216),#32616);
#32726=PRODUCT_DEFINITION_CONTEXT('part definition',#32785,'design');
#32735=PRODUCT_DEFINITION('Flat washer M4','Flat washer M4',#32754,#32726);
#32754=PRODUCT_DEFINITION_FORMATION('',$,#32795);
#32785=APPLICATION_CONTEXT(
'Core Data for Automotive Mechanical Design Process');
#32786=PRODUCT_CONTEXT('part definition',#32785,'mechanical');
#32795=PRODUCT('Flat washer M4','Flat washer M4',$,(#32786));
#32812=PRESENTATION_STYLE_ASSIGNMENT((#32819));
#32819=SURFACE_STYLE_USAGE(.BOTH.,#32826);
#32826=SURFACE_SIDE_STYLE('',(#32833));
#32833=SURFACE_STYLE_FILL_AREA(#32840);
#32840=FILL_AREA_STYLE('Light gray',(#32847));
#32847=FILL_AREA_STYLE_COLOUR('Light gray',#32854);
#32854=COLOUR_RGB('Light gray',0.725490196078431,0.752941176470588,0.792156862745098);
ENDSEC;
END-ISO-10303-21;
